ISO-10303-21;
HEADER;
/* Generated by software containing ST-Developer
 * from STEP Tools, Inc. (www.steptools.com) 
 */

FILE_DESCRIPTION(
/* description */ ('Bracket-mounted idler roller'),
/* implementation_level */ '2;1');

FILE_NAME(
/* name */ 'Cap Screw - M4x16.step',
/* time_stamp */ '2026-10-28T03:26:42-07:00',
/* author */ (''),
/* organization */ (''),
/* preprocessor_version */ 'ST-DEVELOPER v20.2',
/* originating_system */ 'Autodesk Translation Framework v15.17.0.0',
/* authorisation */ '');

FILE_SCHEMA (('AUTOMOTIVE_DESIGN { 1 0 10303 214 3 1 1 }'));
ENDSEC;

DATA;
#10=MECHANICAL_DESIGN_GEOMETRIC_PRESENTATION_REPRESENTATION('',(#308),#6241);
#230=CONICAL_SURFACE('',#3824,0.325,0.785398163397448);
#231=CONICAL_SURFACE('',#3828,0.335,0.785398163397448);
#232=CONICAL_SURFACE('',#3832,0.21,0.463647609000806);
#233=CONICAL_SURFACE('',#3836,0.18,0.785398163397448);
#235=ORIENTED_CLOSED_SHELL('',*,#3212,.F.);
#237=BREP_WITH_VOIDS('Body1',#3211,(#235));
#258=SHAPE_REPRESENTATION_RELATIONSHIP('SRR','None',#6364,#279);
#279=ADVANCED_BREP_SHAPE_REPRESENTATION('',(#237),#6240);
#308=STYLED_ITEM('',(#6545),#237);
#416=FACE_BOUND('',#966,.T.);
#505=PLANE('',#3822);
#506=PLANE('',#3830);
#507=PLANE('',#3838);
#508=PLANE('',#3839);
#509=PLANE('',#3840);
#510=PLANE('',#3841);
#511=PLANE('',#3842);
#512=PLANE('',#3843);
#513=PLANE('',#3844);
#514=PLANE('',#3845);
#515=PLANE('',#3846);
#690=FACE_OUTER_BOUND('',#961,.T.);
#691=FACE_OUTER_BOUND('',#962,.T.);
#692=FACE_OUTER_BOUND('',#963,.T.);
#693=FACE_OUTER_BOUND('',#964,.T.);
#694=FACE_OUTER_BOUND('',#965,.T.);
#695=FACE_OUTER_BOUND('',#967,.T.);
#696=FACE_OUTER_BOUND('',#968,.T.);
#697=FACE_OUTER_BOUND('',#969,.T.);
#698=FACE_OUTER_BOUND('',#970,.T.);
#699=FACE_OUTER_BOUND('',#971,.T.);
#700=FACE_OUTER_BOUND('',#972,.T.);
#701=FACE_OUTER_BOUND('',#973,.T.);
#702=FACE_OUTER_BOUND('',#974,.T.);
#703=FACE_OUTER_BOUND('',#975,.T.);
#704=FACE_OUTER_BOUND('',#976,.T.);
#705=FACE_OUTER_BOUND('',#977,.T.);
#706=FACE_OUTER_BOUND('',#978,.T.);
#961=EDGE_LOOP('',(#2864));
#962=EDGE_LOOP('',(#2865,#2866,#2867,#2868));
#963=EDGE_LOOP('',(#2869,#2870,#2871,#2872));
#964=EDGE_LOOP('',(#2873,#2874,#2875,#2876));
#965=EDGE_LOOP('',(#2877));
#966=EDGE_LOOP('',(#2878));
#967=EDGE_LOOP('',(#2879,#2880,#2881,#2882));
#968=EDGE_LOOP('',(#2883,#2884,#2885,#2886));
#969=EDGE_LOOP('',(#2887,#2888,#2889,#2890));
#970=EDGE_LOOP('',(#2891));
#971=EDGE_LOOP('',(#2892,#2893,#2894,#2895));
#972=EDGE_LOOP('',(#2896,#2897,#2898,#2899));
#973=EDGE_LOOP('',(#2900,#2901,#2902,#2903));
#974=EDGE_LOOP('',(#2904,#2905,#2906,#2907));
#975=EDGE_LOOP('',(#2908,#2909,#2910,#2911));
#976=EDGE_LOOP('',(#2912,#2913,#2914,#2915));
#977=EDGE_LOOP('',(#2916,#2917,#2918,#2919,#2920,#2921));
#978=EDGE_LOOP('',(#2922,#2923,#2924,#2925,#2926,#2927));
#1137=LINE('',#6088,#1319);
#1138=LINE('',#6092,#1320);
#1139=LINE('',#6096,#1321);
#1140=LINE('',#6103,#1322);
#1141=LINE('',#6107,#1323);
#1142=LINE('',#6111,#1324);
#1143=LINE('',#6116,#1325);
#1144=LINE('',#6118,#1326);
#1145=LINE('',#6120,#1327);
#1146=LINE('',#6121,#1328);
#1147=LINE('',#6124,#1329);
#1148=LINE('',#6126,#1330);
#1149=LINE('',#6127,#1331);
#1150=LINE('',#6130,#1332);
#1151=LINE('',#6132,#1333);
#1152=LINE('',#6133,#1334);
#1153=LINE('',#6136,#1335);
#1154=LINE('',#6138,#1336);
#1155=LINE('',#6139,#1337);
#1156=LINE('',#6142,#1338);
#1157=LINE('',#6144,#1339);
#1158=LINE('',#6145,#1340);
#1159=LINE('',#6147,#1341);
#1160=LINE('',#6148,#1342);
#1319=VECTOR('',#4806,0.325);
#1320=VECTOR('',#4811,0.35);
#1321=VECTOR('',#4816,0.335);
#1322=VECTOR('',#4825,0.21);
#1323=VECTOR('',#4830,0.2);
#1324=VECTOR('',#4835,0.18);
#1325=VECTOR('',#4840,1.);
#1326=VECTOR('',#4841,1.);
#1327=VECTOR('',#4842,1.);
#1328=VECTOR('',#4843,1.);
#1329=VECTOR('',#4846,1.);
#1330=VECTOR('',#4847,1.);
#1331=VECTOR('',#4848,1.);
#1332=VECTOR('',#4851,1.);
#1333=VECTOR('',#4852,1.);
#1334=VECTOR('',#4853,1.);
#1335=VECTOR('',#4856,1.);
#1336=VECTOR('',#4857,1.);
#1337=VECTOR('',#4858,1.);
#1338=VECTOR('',#4861,1.);
#1339=VECTOR('',#4862,1.);
#1340=VECTOR('',#4863,1.);
#1341=VECTOR('',#4866,1.);
#1342=VECTOR('',#4867,1.);
#1516=CIRCLE('',#3823,0.3);
#1517=CIRCLE('',#3825,0.35);
#1518=CIRCLE('',#3827,0.35);
#1519=CIRCLE('',#3829,0.32);
#1520=CIRCLE('',#3831,0.22);
#1521=CIRCLE('',#3833,0.1954);
#1522=CIRCLE('',#3835,0.1954);
#1523=CIRCLE('',#3837,0.16);
#1765=VERTEX_POINT('',#6083);
#1766=VERTEX_POINT('',#6086);
#1767=VERTEX_POINT('',#6090);
#1768=VERTEX_POINT('',#6094);
#1769=VERTEX_POINT('',#6098);
#1770=VERTEX_POINT('',#6101);
#1771=VERTEX_POINT('',#6105);
#1772=VERTEX_POINT('',#6109);
#1773=VERTEX_POINT('',#6114);
#1774=VERTEX_POINT('',#6115);
#1775=VERTEX_POINT('',#6117);
#1776=VERTEX_POINT('',#6119);
#1777=VERTEX_POINT('',#6123);
#1778=VERTEX_POINT('',#6125);
#1779=VERTEX_POINT('',#6129);
#1780=VERTEX_POINT('',#6131);
#1781=VERTEX_POINT('',#6135);
#1782=VERTEX_POINT('',#6137);
#1783=VERTEX_POINT('',#6141);
#1784=VERTEX_POINT('',#6143);
#2134=EDGE_CURVE('',#1765,#1765,#1516,.T.);
#2135=EDGE_CURVE('',#1766,#1766,#1517,.T.);
#2136=EDGE_CURVE('',#1766,#1765,#1137,.T.);
#2137=EDGE_CURVE('',#1767,#1767,#1518,.T.);
#2138=EDGE_CURVE('',#1767,#1766,#1138,.T.);
#2139=EDGE_CURVE('',#1768,#1768,#1519,.T.);
#2140=EDGE_CURVE('',#1768,#1767,#1139,.T.);
#2141=EDGE_CURVE('',#1769,#1769,#1520,.T.);
#2142=EDGE_CURVE('',#1770,#1770,#1521,.F.);
#2143=EDGE_CURVE('',#1770,#1769,#1140,.T.);
#2144=EDGE_CURVE('',#1771,#1771,#1522,.F.);
#2145=EDGE_CURVE('',#1771,#1770,#1141,.T.);
#2146=EDGE_CURVE('',#1772,#1772,#1523,.T.);
#2147=EDGE_CURVE('',#1772,#1771,#1142,.T.);
#2148=EDGE_CURVE('',#1773,#1774,#1143,.T.);
#2149=EDGE_CURVE('',#1774,#1775,#1144,.T.);
#2150=EDGE_CURVE('',#1775,#1776,#1145,.T.);
#2151=EDGE_CURVE('',#1773,#1776,#1146,.T.);
#2152=EDGE_CURVE('',#1774,#1777,#1147,.T.);
#2153=EDGE_CURVE('',#1777,#1778,#1148,.T.);
#2154=EDGE_CURVE('',#1778,#1775,#1149,.T.);
#2155=EDGE_CURVE('',#1777,#1779,#1150,.T.);
#2156=EDGE_CURVE('',#1779,#1780,#1151,.T.);
#2157=EDGE_CURVE('',#1780,#1778,#1152,.T.);
#2158=EDGE_CURVE('',#1779,#1781,#1153,.T.);
#2159=EDGE_CURVE('',#1781,#1782,#1154,.T.);
#2160=EDGE_CURVE('',#1782,#1780,#1155,.T.);
#2161=EDGE_CURVE('',#1781,#1783,#1156,.T.);
#2162=EDGE_CURVE('',#1783,#1784,#1157,.T.);
#2163=EDGE_CURVE('',#1784,#1782,#1158,.T.);
#2164=EDGE_CURVE('',#1783,#1773,#1159,.T.);
#2165=EDGE_CURVE('',#1776,#1784,#1160,.T.);
#2864=ORIENTED_EDGE('',*,*,#2134,.F.);
#2865=ORIENTED_EDGE('',*,*,#2135,.F.);
#2866=ORIENTED_EDGE('',*,*,#2136,.T.);
#2867=ORIENTED_EDGE('',*,*,#2134,.T.);
#2868=ORIENTED_EDGE('',*,*,#2136,.F.);
#2869=ORIENTED_EDGE('',*,*,#2137,.F.);
#2870=ORIENTED_EDGE('',*,*,#2138,.T.);
#2871=ORIENTED_EDGE('',*,*,#2135,.T.);
#2872=ORIENTED_EDGE('',*,*,#2138,.F.);
#2873=ORIENTED_EDGE('',*,*,#2139,.F.);
#2874=ORIENTED_EDGE('',*,*,#2140,.T.);
#2875=ORIENTED_EDGE('',*,*,#2137,.T.);
#2876=ORIENTED_EDGE('',*,*,#2140,.F.);
#2877=ORIENTED_EDGE('',*,*,#2139,.T.);
#2878=ORIENTED_EDGE('',*,*,#2141,.F.);
#2879=ORIENTED_EDGE('',*,*,#2142,.F.);
#2880=ORIENTED_EDGE('',*,*,#2143,.T.);
#2881=ORIENTED_EDGE('',*,*,#2141,.T.);
#2882=ORIENTED_EDGE('',*,*,#2143,.F.);
#2883=ORIENTED_EDGE('',*,*,#2144,.F.);
#2884=ORIENTED_EDGE('',*,*,#2145,.T.);
#2885=ORIENTED_EDGE('',*,*,#2142,.T.);
#2886=ORIENTED_EDGE('',*,*,#2145,.F.);
#2887=ORIENTED_EDGE('',*,*,#2146,.F.);
#2888=ORIENTED_EDGE('',*,*,#2147,.T.);
#2889=ORIENTED_EDGE('',*,*,#2144,.T.);
#2890=ORIENTED_EDGE('',*,*,#2147,.F.);
#2891=ORIENTED_EDGE('',*,*,#2146,.T.);
#2892=ORIENTED_EDGE('',*,*,#2148,.T.);
#2893=ORIENTED_EDGE('',*,*,#2149,.T.);
#2894=ORIENTED_EDGE('',*,*,#2150,.T.);
#2895=ORIENTED_EDGE('',*,*,#2151,.F.);
#2896=ORIENTED_EDGE('',*,*,#2152,.T.);
#2897=ORIENTED_EDGE('',*,*,#2153,.T.);
#2898=ORIENTED_EDGE('',*,*,#2154,.T.);
#2899=ORIENTED_EDGE('',*,*,#2149,.F.);
#2900=ORIENTED_EDGE('',*,*,#2155,.T.);
#2901=ORIENTED_EDGE('',*,*,#2156,.T.);
#2902=ORIENTED_EDGE('',*,*,#2157,.T.);
#2903=ORIENTED_EDGE('',*,*,#2153,.F.);
#2904=ORIENTED_EDGE('',*,*,#2158,.T.);
#2905=ORIENTED_EDGE('',*,*,#2159,.T.);
#2906=ORIENTED_EDGE('',*,*,#2160,.T.);
#2907=ORIENTED_EDGE('',*,*,#2156,.F.);
#2908=ORIENTED_EDGE('',*,*,#2161,.T.);
#2909=ORIENTED_EDGE('',*,*,#2162,.T.);
#2910=ORIENTED_EDGE('',*,*,#2163,.T.);
#2911=ORIENTED_EDGE('',*,*,#2159,.F.);
#2912=ORIENTED_EDGE('',*,*,#2164,.T.);
#2913=ORIENTED_EDGE('',*,*,#2151,.T.);
#2914=ORIENTED_EDGE('',*,*,#2165,.T.);
#2915=ORIENTED_EDGE('',*,*,#2162,.F.);
#2916=ORIENTED_EDGE('',*,*,#2164,.F.);
#2917=ORIENTED_EDGE('',*,*,#2161,.F.);
#2918=ORIENTED_EDGE('',*,*,#2158,.F.);
#2919=ORIENTED_EDGE('',*,*,#2155,.F.);
#2920=ORIENTED_EDGE('',*,*,#2152,.F.);
#2921=ORIENTED_EDGE('',*,*,#2148,.F.);
#2922=ORIENTED_EDGE('',*,*,#2165,.F.);
#2923=ORIENTED_EDGE('',*,*,#2150,.F.);
#2924=ORIENTED_EDGE('',*,*,#2154,.F.);
#2925=ORIENTED_EDGE('',*,*,#2157,.F.);
#2926=ORIENTED_EDGE('',*,*,#2160,.F.);
#2927=ORIENTED_EDGE('',*,*,#2163,.F.);
#2989=CYLINDRICAL_SURFACE('',#3826,0.35);
#2990=CYLINDRICAL_SURFACE('',#3834,0.1954);
#3165=ADVANCED_FACE('',(#690),#505,.T.);
#3166=ADVANCED_FACE('',(#691),#230,.T.);
#3167=ADVANCED_FACE('',(#692),#2989,.T.);
#3168=ADVANCED_FACE('',(#693),#231,.T.);
#3169=ADVANCED_FACE('',(#694,#416),#506,.T.);
#3170=ADVANCED_FACE('',(#695),#232,.T.);
#3171=ADVANCED_FACE('',(#696),#2990,.T.);
#3172=ADVANCED_FACE('',(#697),#233,.T.);
#3173=ADVANCED_FACE('',(#698),#507,.T.);
#3174=ADVANCED_FACE('',(#699),#508,.F.);
#3175=ADVANCED_FACE('',(#700),#509,.F.);
#3176=ADVANCED_FACE('',(#701),#510,.F.);
#3177=ADVANCED_FACE('',(#702),#511,.F.);
#3178=ADVANCED_FACE('',(#703),#512,.F.);
#3179=ADVANCED_FACE('',(#704),#513,.F.);
#3180=ADVANCED_FACE('',(#705),#514,.F.);
#3181=ADVANCED_FACE('',(#706),#515,.F.);
#3211=CLOSED_SHELL('',(#3165,#3166,#3167,#3168,#3169,#3170,#3171,#3172,
#3173));
#3212=CLOSED_SHELL('',(#3174,#3175,#3176,#3177,#3178,#3179,#3180,#3181));
#3821=AXIS2_PLACEMENT_3D('',#6081,#4796,#4797);
#3822=AXIS2_PLACEMENT_3D('',#6082,#4798,#4799);
#3823=AXIS2_PLACEMENT_3D('',#6084,#4800,#4801);
#3824=AXIS2_PLACEMENT_3D('',#6085,#4802,#4803);
#3825=AXIS2_PLACEMENT_3D('',#6087,#4804,#4805);
#3826=AXIS2_PLACEMENT_3D('',#6089,#4807,#4808);
#3827=AXIS2_PLACEMENT_3D('',#6091,#4809,#4810);
#3828=AXIS2_PLACEMENT_3D('',#6093,#4812,#4813);
#3829=AXIS2_PLACEMENT_3D('',#6095,#4814,#4815);
#3830=AXIS2_PLACEMENT_3D('',#6097,#4817,#4818);
#3831=AXIS2_PLACEMENT_3D('',#6099,#4819,#4820);
#3832=AXIS2_PLACEMENT_3D('',#6100,#4821,#4822);
#3833=AXIS2_PLACEMENT_3D('',#6102,#4823,#4824);
#3834=AXIS2_PLACEMENT_3D('',#6104,#4826,#4827);
#3835=AXIS2_PLACEMENT_3D('',#6106,#4828,#4829);
#3836=AXIS2_PLACEMENT_3D('',#6108,#4831,#4832);
#3837=AXIS2_PLACEMENT_3D('',#6110,#4833,#4834);
#3838=AXIS2_PLACEMENT_3D('',#6112,#4836,#4837);
#3839=AXIS2_PLACEMENT_3D('',#6113,#4838,#4839);
#3840=AXIS2_PLACEMENT_3D('',#6122,#4844,#4845);
#3841=AXIS2_PLACEMENT_3D('',#6128,#4849,#4850);
#3842=AXIS2_PLACEMENT_3D('',#6134,#4854,#4855);
#3843=AXIS2_PLACEMENT_3D('',#6140,#4859,#4860);
#3844=AXIS2_PLACEMENT_3D('',#6146,#4864,#4865);
#3845=AXIS2_PLACEMENT_3D('',#6149,#4868,#4869);
#3846=AXIS2_PLACEMENT_3D('',#6150,#4870,#4871);
#4796=DIRECTION('axis',(0.,0.,1.));
#4797=DIRECTION('refdir',(1.,0.,0.));
#4798=DIRECTION('center_axis',(0.,1.,0.));
#4799=DIRECTION('ref_axis',(0.,0.,1.));
#4800=DIRECTION('center_axis',(0.,-1.,0.));
#4801=DIRECTION('ref_axis',(1.,0.,0.));
#4802=DIRECTION('center_axis',(0.,-1.,0.));
#4803=DIRECTION('ref_axis',(1.,0.,0.));
#4804=DIRECTION('center_axis',(0.,-1.,0.));
#4805=DIRECTION('ref_axis',(1.,0.,0.));
#4806=DIRECTION('',(0.707106781186547,0.707106781186548,8.65956056235493E-17));
#4807=DIRECTION('center_axis',(0.,-1.,0.));
#4808=DIRECTION('ref_axis',(1.,0.,0.));
#4809=DIRECTION('center_axis',(0.,-1.,0.));
#4810=DIRECTION('ref_axis',(1.,0.,0.));
#4811=DIRECTION('',(0.,1.,0.));
#4812=DIRECTION('center_axis',(0.,1.,0.));
#4813=DIRECTION('ref_axis',(1.,0.,0.));
#4814=DIRECTION('center_axis',(0.,-1.,0.));
#4815=DIRECTION('ref_axis',(1.,0.,0.));
#4816=DIRECTION('',(-0.707106781186547,0.707106781186548,-8.65956056235493E-17));
#4817=DIRECTION('center_axis',(0.,-1.,0.));
#4818=DIRECTION('ref_axis',(0.,0.,-1.));
#4819=DIRECTION('center_axis',(0.,-1.,0.));
#4820=DIRECTION('ref_axis',(1.,0.,0.));
#4821=DIRECTION('center_axis',(0.,1.,0.));
#4822=DIRECTION('ref_axis',(1.,0.,0.));
#4823=DIRECTION('center_axis',(0.,1.,0.));
#4824=DIRECTION('ref_axis',(1.,0.,0.));
#4825=DIRECTION('',(-0.447213595499958,0.894427190999916,-5.47678698264203E-17));
#4826=DIRECTION('center_axis',(0.,-1.,0.));
#4827=DIRECTION('ref_axis',(1.,0.,0.));
#4828=DIRECTION('center_axis',(0.,1.,0.));
#4829=DIRECTION('ref_axis',(1.,0.,0.));
#4830=DIRECTION('',(0.,1.,0.));
#4831=DIRECTION('center_axis',(0.,1.,0.));
#4832=DIRECTION('ref_axis',(1.,0.,0.));
#4833=DIRECTION('center_axis',(0.,-1.,0.));
#4834=DIRECTION('ref_axis',(1.,0.,0.));
#4835=DIRECTION('',(-0.707106781186547,0.707106781186548,-8.65956056235493E-17));
#4836=DIRECTION('center_axis',(0.,-1.,0.));
#4837=DIRECTION('ref_axis',(0.,0.,-1.));
#4838=DIRECTION('center_axis',(0.866025403784439,0.,-0.5));
#4839=DIRECTION('ref_axis',(0.5,0.,0.866025403784439));
#4840=DIRECTION('',(-0.5,0.,-0.866025403784439));
#4841=DIRECTION('',(0.,-1.,0.));
#4842=DIRECTION('',(0.5,0.,0.866025403784439));
#4843=DIRECTION('',(0.,-1.,0.));
#4844=DIRECTION('center_axis',(1.60246890531964E-16,0.,-1.));
#4845=DIRECTION('ref_axis',(1.,0.,1.60246890531964E-16));
#4846=DIRECTION('',(-1.,0.,-1.60246890531964E-16));
#4847=DIRECTION('',(0.,-1.,0.));
#4848=DIRECTION('',(1.,0.,1.60246890531964E-16));
#4849=DIRECTION('center_axis',(-0.866025403784439,0.,-0.5));
#4850=DIRECTION('ref_axis',(0.5,0.,-0.866025403784439));
#4851=DIRECTION('',(-0.5,0.,0.866025403784439));
#4852=DIRECTION('',(0.,-1.,0.));
#4853=DIRECTION('',(0.5,0.,-0.866025403784439));
#4854=DIRECTION('center_axis',(-0.866025403784439,0.,0.5));
#4855=DIRECTION('ref_axis',(-0.5,0.,-0.866025403784439));
#4856=DIRECTION('',(0.5,0.,0.866025403784439));
#4857=DIRECTION('',(0.,-1.,0.));
#4858=DIRECTION('',(-0.5,0.,-0.866025403784439));
#4859=DIRECTION('center_axis',(-1.60246890531964E-16,0.,1.));
#4860=DIRECTION('ref_axis',(-1.,0.,-1.60246890531964E-16));
#4861=DIRECTION('',(1.,0.,1.60246890531964E-16));
#4862=DIRECTION('',(0.,-1.,0.));
#4863=DIRECTION('',(-1.,0.,-1.60246890531964E-16));
#4864=DIRECTION('center_axis',(0.866025403784439,0.,0.5));
#4865=DIRECTION('ref_axis',(-0.5,0.,0.866025403784439));
#4866=DIRECTION('',(0.5,0.,-0.866025403784439));
#4867=DIRECTION('',(-0.5,0.,0.866025403784439));
#4868=DIRECTION('center_axis',(0.,1.,0.));
#4869=DIRECTION('ref_axis',(1.,0.,0.));
#4870=DIRECTION('center_axis',(0.,-1.,0.));
#4871=DIRECTION('ref_axis',(0.,0.,-1.));
#6081=CARTESIAN_POINT('',(0.,0.,0.));
#6082=CARTESIAN_POINT('Origin',(0.3,0.4,0.));
#6083=CARTESIAN_POINT('',(-0.3,0.4,-3.67394039744206E-17));
#6084=CARTESIAN_POINT('Origin',(0.,0.4,0.));
#6085=CARTESIAN_POINT('Origin',(0.,0.375,0.));
#6086=CARTESIAN_POINT('',(-0.35,0.35,-4.28626379701573E-17));
#6087=CARTESIAN_POINT('Origin',(0.,0.35,0.));
#6088=CARTESIAN_POINT('',(-0.325,0.375,-3.9801020972289E-17));
#6089=CARTESIAN_POINT('Origin',(0.,0.19,0.));
#6090=CARTESIAN_POINT('',(-0.35,0.03,-4.28626379701574E-17));
#6091=CARTESIAN_POINT('Origin',(0.,0.03,0.));
#6092=CARTESIAN_POINT('',(-0.35,0.19,-4.28626379701574E-17));
#6093=CARTESIAN_POINT('Origin',(0.,0.0149999999999999,0.));
#6094=CARTESIAN_POINT('',(-0.32,-3.29597460435593E-17,-3.91886975727153E-17));
#6095=CARTESIAN_POINT('Origin',(0.,0.,0.));
#6096=CARTESIAN_POINT('',(-0.335,0.0149999999999999,-4.10256677714363E-17));
#6097=CARTESIAN_POINT('Origin',(0.22,0.,0.));
#6098=CARTESIAN_POINT('',(-0.22,-6.93889390390723E-18,-2.69422295812418E-17));
#6099=CARTESIAN_POINT('Origin',(0.,0.,0.));
#6100=CARTESIAN_POINT('Origin',(0.,-0.02,0.));
#6101=CARTESIAN_POINT('',(-0.1954,-0.0492,2.39295984553393E-17));
#6102=CARTESIAN_POINT('Origin',(0.,-0.0492,0.));
#6103=CARTESIAN_POINT('',(-0.21,-0.02,-2.57175827820944E-17));
#6104=CARTESIAN_POINT('Origin',(0.,-0.8,0.));
#6105=CARTESIAN_POINT('',(-0.1954,-1.5646,2.39295984553393E-17));
#6106=CARTESIAN_POINT('Origin',(0.,-1.5646,0.));
#6107=CARTESIAN_POINT('',(-0.1954,-0.8,-2.39295984553393E-17));
#6108=CARTESIAN_POINT('Origin',(0.,-1.58,0.));
#6109=CARTESIAN_POINT('',(-0.16,-1.6,-1.95943487863577E-17));
#6110=CARTESIAN_POINT('Origin',(0.,-1.6,0.));
#6111=CARTESIAN_POINT('',(-0.18,-1.58,-2.20436423846524E-17));
#6112=CARTESIAN_POINT('Origin',(0.,-1.6,0.));
#6113=CARTESIAN_POINT('Origin',(0.0866025403784439,-0.4,-0.15));
#6114=CARTESIAN_POINT('',(0.173205080756888,-0.4,0.));
#6115=CARTESIAN_POINT('',(0.0866025403784439,-0.4,-0.15));
#6116=CARTESIAN_POINT('',(0.173205080756888,-0.4,0.));
#6117=CARTESIAN_POINT('',(0.0866025403784439,-0.64,-0.15));
#6118=CARTESIAN_POINT('',(0.0866025403784439,-0.4,-0.15));
#6119=CARTESIAN_POINT('',(0.173205080756888,-0.64,0.));
#6120=CARTESIAN_POINT('',(0.173205080756888,-0.64,0.));
#6121=CARTESIAN_POINT('',(0.173205080756888,-0.4,0.));
#6122=CARTESIAN_POINT('Origin',(-0.0866025403784438,-0.4,-0.15));
#6123=CARTESIAN_POINT('',(-0.0866025403784438,-0.4,-0.15));
#6124=CARTESIAN_POINT('',(0.0866025403784439,-0.4,-0.15));
#6125=CARTESIAN_POINT('',(-0.0866025403784438,-0.64,-0.15));
#6126=CARTESIAN_POINT('',(-0.0866025403784438,-0.4,-0.15));
#6127=CARTESIAN_POINT('',(0.0866025403784439,-0.64,-0.15));
#6128=CARTESIAN_POINT('Origin',(-0.173205080756888,-0.4,-2.77555756156289E-17));
#6129=CARTESIAN_POINT('',(-0.173205080756888,-0.4,-2.12115047744981E-17));
#6130=CARTESIAN_POINT('',(-0.0866025403784438,-0.4,-0.15));
#6131=CARTESIAN_POINT('',(-0.173205080756888,-0.64,-2.77555756156289E-17));
#6132=CARTESIAN_POINT('',(-0.173205080756888,-0.4,-2.12115047744981E-17));
#6133=CARTESIAN_POINT('',(-0.0866025403784438,-0.64,-0.15));
#6134=CARTESIAN_POINT('Origin',(-0.0866025403784439,-0.4,0.15));
#6135=CARTESIAN_POINT('',(-0.0866025403784439,-0.4,0.15));
#6136=CARTESIAN_POINT('',(-0.173205080756888,-0.4,-2.12115047744981E-17));
#6137=CARTESIAN_POINT('',(-0.0866025403784439,-0.64,0.15));
#6138=CARTESIAN_POINT('',(-0.0866025403784439,-0.4,0.15));
#6139=CARTESIAN_POINT('',(-0.173205080756888,-0.64,-2.12115047744981E-17));
#6140=CARTESIAN_POINT('Origin',(0.0866025403784439,-0.4,0.15));
#6141=CARTESIAN_POINT('',(0.0866025403784439,-0.4,0.15));
#6142=CARTESIAN_POINT('',(-0.0866025403784439,-0.4,0.15));
#6143=CARTESIAN_POINT('',(0.0866025403784439,-0.64,0.15));
#6144=CARTESIAN_POINT('',(0.0866025403784439,-0.4,0.15));
#6145=CARTESIAN_POINT('',(-0.0866025403784439,-0.64,0.15));
#6146=CARTESIAN_POINT('Origin',(0.173205080756888,-0.4,0.));
#6147=CARTESIAN_POINT('',(0.0866025403784439,-0.4,0.15));
#6148=CARTESIAN_POINT('',(0.0866025403784439,-0.64,0.15));
#6149=CARTESIAN_POINT('Origin',(0.,-0.4,-2.77555756156289E-17));
#6150=CARTESIAN_POINT('Origin',(0.,-0.64,-2.77555756156289E-17));
#6214=UNCERTAINTY_MEASURE_WITH_UNIT(LENGTH_MEASURE(0.001),#6242,
'DISTANCE_ACCURACY_VALUE',
'Maximum model space distance between geometric entities at asserted c
onnectivities');
#6215=UNCERTAINTY_MEASURE_WITH_UNIT(LENGTH_MEASURE(0.001),#6242,
'DISTANCE_ACCURACY_VALUE',
'Maximum model space distance between geometric entities at asserted c
onnectivities');
#6240=(
GEOMETRIC_REPRESENTATION_CONTEXT(3)
GLOBAL_UNCERTAINTY_ASSIGNED_CONTEXT((#6214))
GLOBAL_UNIT_ASSIGNED_CONTEXT((#6242,#6244,#6245))
REPRESENTATION_CONTEXT('','3D')
);
#6241=(
GEOMETRIC_REPRESENTATION_CONTEXT(3)
GLOBAL_UNCERTAINTY_ASSIGNED_CONTEXT((#6215))
GLOBAL_UNIT_ASSIGNED_CONTEXT((#6242,#6244,#6245))
REPRESENTATION_CONTEXT('','3D')
);
#6242=(
LENGTH_UNIT()
NAMED_UNIT(*)
SI_UNIT(.CENTI.,.METRE.)
);
#6244=(
NAMED_UNIT(*)
PLANE_ANGLE_UNIT()
SI_UNIT($,.RADIAN.)
);
#6245=(
NAMED_UNIT(*)
SI_UNIT($,.STERADIAN.)
SOLID_ANGLE_UNIT()
);
#6270=SHAPE_DEFINITION_REPRESENTATION(#6300,#6364);
#6300=PRODUCT_DEFINITION_SHAPE('',$,#6390);
#6364=SHAPE_REPRESENTATION('',(#3821),#6240);
#6365=PRODUCT_DEFINITION_CONTEXT('part definition',#6442,'design');
#6390=PRODUCT_DEFINITION('Cap Screw - M4x16','Cap Screw - M4x16',#6415,
#6365);
#6415=PRODUCT_DEFINITION_FORMATION('',$,#6468);
#6442=APPLICATION_CONTEXT(
'Core Data for Automotive Mechanical Design Process');
#6443=PRODUCT_CONTEXT('part definition',#6442,'mechanical');
#6468=PRODUCT('Cap Screw - M4x16','Cap Screw - M4x16',
'Cap Screw - M4x16',(#6443));
#6539=COLOUR_RGB('Black',0.12,0.14,0.17);
#6540=FILL_AREA_STYLE_COLOUR('',#6539);
#6541=FILL_AREA_STYLE('',(#6540));
#6542=SURFACE_STYLE_FILL_AREA(#6541);
#6543=SURFACE_SIDE_STYLE('',(#6542));
#6544=SURFACE_STYLE_USAGE(.BOTH.,#6543);
#6545=PRESENTATION_STYLE_ASSIGNMENT((#6544));
ENDSEC;
END-ISO-10303-21;
